ISO-10303-21;
HEADER;
/* Generated by software containing ST-Developer
 * from STEP Tools, Inc. (www.steptools.com) 
 */

FILE_DESCRIPTION(
/* description */ (''),
/* implementation_level */ '2;1');

FILE_NAME(
/* name */ '11_Handle_Pin_D6x22.step',
/* time_stamp */ '2026-10-26T03:55:20-07:00',
/* author */ (''),
/* organization */ (''),
/* preprocessor_version */ 'ST-DEVELOPER v20.2',
/* originating_system */ 'Autodesk Translation Framework v15.15.0.0',
/* authorisation */ '');

FILE_SCHEMA (('AUTOMOTIVE_DESIGN { 1 0 10303 214 3 1 1 }'));
ENDSEC;

DATA;
#10=MECHANICAL_DESIGN_GEOMETRIC_PRESENTATION_REPRESENTATION('',(#183),#45236);
#143=SHAPE_REPRESENTATION_RELATIONSHIP('SRR','None',#45322,#163);
#163=ADVANCED_BREP_SHAPE_REPRESENTATION('',(#203),#45224);
#183=STYLED_ITEM('',(#45484),#203);
#203=MANIFOLD_SOLID_BREP('Body1',#16525);
#970=FACE_BOUND('',#3232,.T.);
#971=FACE_BOUND('',#3235,.T.);
#972=FACE_BOUND('',#3238,.T.);
#973=FACE_BOUND('',#3241,.T.);
#1213=PLANE('',#17254);
#1214=PLANE('',#17260);
#1215=PLANE('',#17264);
#1216=PLANE('',#17268);
#1217=PLANE('',#17272);
#1218=PLANE('',#17278);
#1684=CYLINDRICAL_SURFACE('',#17258,3.);
#1685=CYLINDRICAL_SURFACE('',#17262,2.5);
#1686=CYLINDRICAL_SURFACE('',#17266,3.);
#1687=CYLINDRICAL_SURFACE('',#17270,2.5);
#1688=CYLINDRICAL_SURFACE('',#17274,3.);
#2223=FACE_OUTER_BOUND('',#3228,.T.);
#2224=FACE_OUTER_BOUND('',#3229,.T.);
#2225=FACE_OUTER_BOUND('',#3230,.T.);
#2226=FACE_OUTER_BOUND('',#3231,.T.);
#2227=FACE_OUTER_BOUND('',#3233,.T.);
#2228=FACE_OUTER_BOUND('',#3234,.T.);
#2229=FACE_OUTER_BOUND('',#3236,.T.);
#2230=FACE_OUTER_BOUND('',#3237,.T.);
#2231=FACE_OUTER_BOUND('',#3239,.T.);
#2232=FACE_OUTER_BOUND('',#3240,.T.);
#2233=FACE_OUTER_BOUND('',#3242,.T.);
#2234=FACE_OUTER_BOUND('',#3243,.T.);
#2235=FACE_OUTER_BOUND('',#3244,.T.);
#3228=EDGE_LOOP('',(#12830));
#3229=EDGE_LOOP('',(#12831,#12832,#12833,#12834));
#3230=EDGE_LOOP('',(#12835,#12836,#12837,#12838));
#3231=EDGE_LOOP('',(#12839));
#3232=EDGE_LOOP('',(#12840));
#3233=EDGE_LOOP('',(#12841,#12842,#12843,#12844));
#3234=EDGE_LOOP('',(#12845));
#3235=EDGE_LOOP('',(#12846));
#3236=EDGE_LOOP('',(#12847,#12848,#12849,#12850));
#3237=EDGE_LOOP('',(#12851));
#3238=EDGE_LOOP('',(#12852));
#3239=EDGE_LOOP('',(#12853,#12854,#12855,#12856));
#3240=EDGE_LOOP('',(#12857));
#3241=EDGE_LOOP('',(#12858));
#3242=EDGE_LOOP('',(#12859,#12860,#12861,#12862));
#3243=EDGE_LOOP('',(#12863,#12864,#12865,#12866));
#3244=EDGE_LOOP('',(#12867));
#4414=LINE('',#33350,#5725);
#4415=LINE('',#33354,#5726);
#4416=LINE('',#33361,#5727);
#4417=LINE('',#33368,#5728);
#4418=LINE('',#33375,#5729);
#4419=LINE('',#33382,#5730);
#4420=LINE('',#33386,#5731);
#5725=VECTOR('',#19651,2.8);
#5726=VECTOR('',#19656,3.);
#5727=VECTOR('',#19665,2.5);
#5728=VECTOR('',#19674,3.);
#5729=VECTOR('',#19683,2.5);
#5730=VECTOR('',#19692,3.);
#5731=VECTOR('',#19697,2.8);
#6673=CIRCLE('',#17255,2.6);
#6674=CIRCLE('',#17257,3.);
#6675=CIRCLE('',#17259,3.);
#6676=CIRCLE('',#17261,2.5);
#6677=CIRCLE('',#17263,2.5);
#6678=CIRCLE('',#17265,3.);
#6679=CIRCLE('',#17267,3.);
#6680=CIRCLE('',#17269,2.5);
#6681=CIRCLE('',#17271,2.5);
#6682=CIRCLE('',#17273,3.);
#6683=CIRCLE('',#17275,3.);
#6684=CIRCLE('',#17277,2.6);
#7606=VERTEX_POINT('',#33345);
#7607=VERTEX_POINT('',#33348);
#7608=VERTEX_POINT('',#33352);
#7609=VERTEX_POINT('',#33356);
#7610=VERTEX_POINT('',#33359);
#7611=VERTEX_POINT('',#33363);
#7612=VERTEX_POINT('',#33366);
#7613=VERTEX_POINT('',#33370);
#7614=VERTEX_POINT('',#33373);
#7615=VERTEX_POINT('',#33377);
#7616=VERTEX_POINT('',#33380);
#7617=VERTEX_POINT('',#33384);
#9478=EDGE_CURVE('',#7606,#7606,#6673,.T.);
#9479=EDGE_CURVE('',#7607,#7607,#6674,.T.);
#9480=EDGE_CURVE('',#7607,#7606,#4414,.T.);
#9481=EDGE_CURVE('',#7608,#7608,#6675,.T.);
#9482=EDGE_CURVE('',#7608,#7607,#4415,.T.);
#9483=EDGE_CURVE('',#7609,#7609,#6676,.T.);
#9484=EDGE_CURVE('',#7610,#7610,#6677,.T.);
#9485=EDGE_CURVE('',#7610,#7609,#4416,.T.);
#9486=EDGE_CURVE('',#7611,#7611,#6678,.T.);
#9487=EDGE_CURVE('',#7612,#7612,#6679,.T.);
#9488=EDGE_CURVE('',#7612,#7611,#4417,.T.);
#9489=EDGE_CURVE('',#7613,#7613,#6680,.T.);
#9490=EDGE_CURVE('',#7614,#7614,#6681,.T.);
#9491=EDGE_CURVE('',#7614,#7613,#4418,.T.);
#9492=EDGE_CURVE('',#7615,#7615,#6682,.T.);
#9493=EDGE_CURVE('',#7616,#7616,#6683,.T.);
#9494=EDGE_CURVE('',#7616,#7615,#4419,.T.);
#9495=EDGE_CURVE('',#7617,#7617,#6684,.T.);
#9496=EDGE_CURVE('',#7617,#7616,#4420,.T.);
#12830=ORIENTED_EDGE('',*,*,#9478,.F.);
#12831=ORIENTED_EDGE('',*,*,#9479,.F.);
#12832=ORIENTED_EDGE('',*,*,#9480,.T.);
#12833=ORIENTED_EDGE('',*,*,#9478,.T.);
#12834=ORIENTED_EDGE('',*,*,#9480,.F.);
#12835=ORIENTED_EDGE('',*,*,#9481,.F.);
#12836=ORIENTED_EDGE('',*,*,#9482,.T.);
#12837=ORIENTED_EDGE('',*,*,#9479,.T.);
#12838=ORIENTED_EDGE('',*,*,#9482,.F.);
#12839=ORIENTED_EDGE('',*,*,#9481,.T.);
#12840=ORIENTED_EDGE('',*,*,#9483,.F.);
#12841=ORIENTED_EDGE('',*,*,#9484,.F.);
#12842=ORIENTED_EDGE('',*,*,#9485,.T.);
#12843=ORIENTED_EDGE('',*,*,#9483,.T.);
#12844=ORIENTED_EDGE('',*,*,#9485,.F.);
#12845=ORIENTED_EDGE('',*,*,#9486,.F.);
#12846=ORIENTED_EDGE('',*,*,#9484,.T.);
#12847=ORIENTED_EDGE('',*,*,#9487,.F.);
#12848=ORIENTED_EDGE('',*,*,#9488,.T.);
#12849=ORIENTED_EDGE('',*,*,#9486,.T.);
#12850=ORIENTED_EDGE('',*,*,#9488,.F.);
#12851=ORIENTED_EDGE('',*,*,#9487,.T.);
#12852=ORIENTED_EDGE('',*,*,#9489,.F.);
#12853=ORIENTED_EDGE('',*,*,#9490,.F.);
#12854=ORIENTED_EDGE('',*,*,#9491,.T.);
#12855=ORIENTED_EDGE('',*,*,#9489,.T.);
#12856=ORIENTED_EDGE('',*,*,#9491,.F.);
#12857=ORIENTED_EDGE('',*,*,#9492,.F.);
#12858=ORIENTED_EDGE('',*,*,#9490,.T.);
#12859=ORIENTED_EDGE('',*,*,#9493,.F.);
#12860=ORIENTED_EDGE('',*,*,#9494,.T.);
#12861=ORIENTED_EDGE('',*,*,#9492,.T.);
#12862=ORIENTED_EDGE('',*,*,#9494,.F.);
#12863=ORIENTED_EDGE('',*,*,#9495,.F.);
#12864=ORIENTED_EDGE('',*,*,#9496,.T.);
#12865=ORIENTED_EDGE('',*,*,#9493,.T.);
#12866=ORIENTED_EDGE('',*,*,#9496,.F.);
#12867=ORIENTED_EDGE('',*,*,#9495,.T.);
#15500=CONICAL_SURFACE('',#17256,2.8,0.785398163397448);
#15501=CONICAL_SURFACE('',#17276,2.8,0.785398163397448);
#15951=ADVANCED_FACE('',(#2223),#1213,.T.);
#15952=ADVANCED_FACE('',(#2224),#15500,.T.);
#15953=ADVANCED_FACE('',(#2225),#1684,.T.);
#15954=ADVANCED_FACE('',(#2226,#970),#1214,.T.);
#15955=ADVANCED_FACE('',(#2227),#1685,.T.);
#15956=ADVANCED_FACE('',(#2228,#971),#1215,.T.);
#15957=ADVANCED_FACE('',(#2229),#1686,.T.);
#15958=ADVANCED_FACE('',(#2230,#972),#1216,.T.);
#15959=ADVANCED_FACE('',(#2231),#1687,.T.);
#15960=ADVANCED_FACE('',(#2232,#973),#1217,.T.);
#15961=ADVANCED_FACE('',(#2233),#1688,.T.);
#15962=ADVANCED_FACE('',(#2234),#15501,.T.);
#15963=ADVANCED_FACE('',(#2235),#1218,.T.);
#16525=CLOSED_SHELL('',(#15951,#15952,#15953,#15954,#15955,#15956,#15957,
#15958,#15959,#15960,#15961,#15962,#15963));
#17253=AXIS2_PLACEMENT_3D('',#33343,#19641,#19642);
#17254=AXIS2_PLACEMENT_3D('',#33344,#19643,#19644);
#17255=AXIS2_PLACEMENT_3D('',#33346,#19645,#19646);
#17256=AXIS2_PLACEMENT_3D('',#33347,#19647,#19648);
#17257=AXIS2_PLACEMENT_3D('',#33349,#19649,#19650);
#17258=AXIS2_PLACEMENT_3D('',#33351,#19652,#19653);
#17259=AXIS2_PLACEMENT_3D('',#33353,#19654,#19655);
#17260=AXIS2_PLACEMENT_3D('',#33355,#19657,#19658);
#17261=AXIS2_PLACEMENT_3D('',#33357,#19659,#19660);
#17262=AXIS2_PLACEMENT_3D('',#33358,#19661,#19662);
#17263=AXIS2_PLACEMENT_3D('',#33360,#19663,#19664);
#17264=AXIS2_PLACEMENT_3D('',#33362,#19666,#19667);
#17265=AXIS2_PLACEMENT_3D('',#33364,#19668,#19669);
#17266=AXIS2_PLACEMENT_3D('',#33365,#19670,#19671);
#17267=AXIS2_PLACEMENT_3D('',#33367,#19672,#19673);
#17268=AXIS2_PLACEMENT_3D('',#33369,#19675,#19676);
#17269=AXIS2_PLACEMENT_3D('',#33371,#19677,#19678);
#17270=AXIS2_PLACEMENT_3D('',#33372,#19679,#19680);
#17271=AXIS2_PLACEMENT_3D('',#33374,#19681,#19682);
#17272=AXIS2_PLACEMENT_3D('',#33376,#19684,#19685);
#17273=AXIS2_PLACEMENT_3D('',#33378,#19686,#19687);
#17274=AXIS2_PLACEMENT_3D('',#33379,#19688,#19689);
#17275=AXIS2_PLACEMENT_3D('',#33381,#19690,#19691);
#17276=AXIS2_PLACEMENT_3D('',#33383,#19693,#19694);
#17277=AXIS2_PLACEMENT_3D('',#33385,#19695,#19696);
#17278=AXIS2_PLACEMENT_3D('',#33387,#19698,#19699);
#19641=DIRECTION('axis',(0.,0.,1.));
#19642=DIRECTION('refdir',(1.,0.,0.));
#19643=DIRECTION('center_axis',(-1.,0.,0.));
#19644=DIRECTION('ref_axis',(0.,0.,1.));
#19645=DIRECTION('center_axis',(1.,0.,0.));
#19646=DIRECTION('ref_axis',(0.,0.,-1.));
#19647=DIRECTION('center_axis',(1.,0.,0.));
#19648=DIRECTION('ref_axis',(0.,1.,0.));
#19649=DIRECTION('center_axis',(1.,0.,0.));
#19650=DIRECTION('ref_axis',(0.,0.,-1.));
#19651=DIRECTION('',(-0.707106781186548,0.707106781186547,8.65956056235493E-17));
#19652=DIRECTION('center_axis',(1.,0.,0.));
#19653=DIRECTION('ref_axis',(0.,1.,0.));
#19654=DIRECTION('center_axis',(1.,0.,0.));
#19655=DIRECTION('ref_axis',(0.,0.,-1.));
#19656=DIRECTION('',(-1.,0.,0.));
#19657=DIRECTION('center_axis',(1.,0.,0.));
#19658=DIRECTION('ref_axis',(0.,0.,-1.));
#19659=DIRECTION('center_axis',(1.,0.,0.));
#19660=DIRECTION('ref_axis',(0.,0.,-1.));
#19661=DIRECTION('center_axis',(1.,0.,0.));
#19662=DIRECTION('ref_axis',(0.,1.,0.));
#19663=DIRECTION('center_axis',(1.,0.,0.));
#19664=DIRECTION('ref_axis',(0.,0.,-1.));
#19665=DIRECTION('',(-1.,0.,0.));
#19666=DIRECTION('center_axis',(-1.,0.,0.));
#19667=DIRECTION('ref_axis',(0.,0.,1.));
#19668=DIRECTION('center_axis',(1.,0.,0.));
#19669=DIRECTION('ref_axis',(0.,0.,-1.));
#19670=DIRECTION('center_axis',(1.,0.,0.));
#19671=DIRECTION('ref_axis',(0.,1.,0.));
#19672=DIRECTION('center_axis',(1.,0.,0.));
#19673=DIRECTION('ref_axis',(0.,0.,-1.));
#19674=DIRECTION('',(-1.,0.,0.));
#19675=DIRECTION('center_axis',(1.,0.,0.));
#19676=DIRECTION('ref_axis',(0.,0.,-1.));
#19677=DIRECTION('center_axis',(1.,0.,0.));
#19678=DIRECTION('ref_axis',(0.,0.,-1.));
#19679=DIRECTION('center_axis',(1.,0.,0.));
#19680=DIRECTION('ref_axis',(0.,1.,0.));
#19681=DIRECTION('center_axis',(1.,0.,0.));
#19682=DIRECTION('ref_axis',(0.,0.,-1.));
#19683=DIRECTION('',(-1.,0.,0.));
#19684=DIRECTION('center_axis',(-1.,0.,0.));
#19685=DIRECTION('ref_axis',(0.,0.,1.));
#19686=DIRECTION('center_axis',(1.,0.,0.));
#19687=DIRECTION('ref_axis',(0.,0.,-1.));
#19688=DIRECTION('center_axis',(1.,0.,0.));
#19689=DIRECTION('ref_axis',(0.,1.,0.));
#19690=DIRECTION('center_axis',(1.,0.,0.));
#19691=DIRECTION('ref_axis',(0.,0.,-1.));
#19692=DIRECTION('',(-1.,0.,0.));
#19693=DIRECTION('center_axis',(-1.,0.,0.));
#19694=DIRECTION('ref_axis',(0.,1.,0.));
#19695=DIRECTION('center_axis',(1.,0.,0.));
#19696=DIRECTION('ref_axis',(0.,0.,-1.));
#19697=DIRECTION('',(-0.707106781186548,-0.707106781186547,-8.65956056235493E-17));
#19698=DIRECTION('center_axis',(1.,0.,0.));
#19699=DIRECTION('ref_axis',(0.,0.,-1.));
#33343=CARTESIAN_POINT('',(0.,0.,0.));
#33344=CARTESIAN_POINT('Origin',(-11.,2.6,0.));
#33345=CARTESIAN_POINT('',(-11.,-2.6,-3.18408167778312E-16));
#33346=CARTESIAN_POINT('Origin',(-11.,0.,0.));
#33347=CARTESIAN_POINT('Origin',(-10.8,0.,0.));
#33348=CARTESIAN_POINT('',(-10.6,-3.,-3.67394039744206E-16));
#33349=CARTESIAN_POINT('Origin',(-10.6,0.,0.));
#33350=CARTESIAN_POINT('',(-10.8,-2.8,-3.42901103761259E-16));
#33351=CARTESIAN_POINT('Origin',(-9.695,0.,0.));
#33352=CARTESIAN_POINT('',(-8.79,-3.,-3.67394039744206E-16));
#33353=CARTESIAN_POINT('Origin',(-8.79,0.,0.));
#33354=CARTESIAN_POINT('',(-9.695,-3.,-3.67394039744206E-16));
#33355=CARTESIAN_POINT('Origin',(-8.79,2.5,0.));
#33356=CARTESIAN_POINT('',(-8.79,-2.5,-3.06161699786838E-16));
#33357=CARTESIAN_POINT('Origin',(-8.79,0.,0.));
#33358=CARTESIAN_POINT('Origin',(-8.42,0.,0.));
#33359=CARTESIAN_POINT('',(-8.05,-2.5,-3.06161699786838E-16));
#33360=CARTESIAN_POINT('Origin',(-8.05,0.,0.));
#33361=CARTESIAN_POINT('',(-8.42,-2.5,-3.06161699786838E-16));
#33362=CARTESIAN_POINT('Origin',(-8.05,3.,0.));
#33363=CARTESIAN_POINT('',(-8.05,-3.,-3.67394039744206E-16));
#33364=CARTESIAN_POINT('Origin',(-8.05,0.,0.));
#33365=CARTESIAN_POINT('Origin',(0.,0.,0.));
#33366=CARTESIAN_POINT('',(8.05,-3.,-3.67394039744206E-16));
#33367=CARTESIAN_POINT('Origin',(8.05,0.,0.));
#33368=CARTESIAN_POINT('',(0.,-3.,-3.67394039744206E-16));
#33369=CARTESIAN_POINT('Origin',(8.05,2.5,0.));
#33370=CARTESIAN_POINT('',(8.05,-2.5,-3.06161699786838E-16));
#33371=CARTESIAN_POINT('Origin',(8.05,0.,0.));
#33372=CARTESIAN_POINT('Origin',(8.42,0.,0.));
#33373=CARTESIAN_POINT('',(8.79,-2.5,-3.06161699786838E-16));
#33374=CARTESIAN_POINT('Origin',(8.79,0.,0.));
#33375=CARTESIAN_POINT('',(8.42,-2.5,-3.06161699786838E-16));
#33376=CARTESIAN_POINT('Origin',(8.79,3.,0.));
#33377=CARTESIAN_POINT('',(8.79,-3.,-3.67394039744206E-16));
#33378=CARTESIAN_POINT('Origin',(8.79,0.,0.));
#33379=CARTESIAN_POINT('Origin',(9.695,0.,0.));
#33380=CARTESIAN_POINT('',(10.6,-3.,-3.67394039744206E-16));
#33381=CARTESIAN_POINT('Origin',(10.6,0.,0.));
#33382=CARTESIAN_POINT('',(9.695,-3.,-3.67394039744206E-16));
#33383=CARTESIAN_POINT('Origin',(10.8,0.,0.));
#33384=CARTESIAN_POINT('',(11.,-2.6,-3.18408167778312E-16));
#33385=CARTESIAN_POINT('Origin',(11.,0.,0.));
#33386=CARTESIAN_POINT('',(10.8,-2.8,-3.42901103761259E-16));
#33387=CARTESIAN_POINT('Origin',(11.,0.,0.));
#45202=UNCERTAINTY_MEASURE_WITH_UNIT(LENGTH_MEASURE(0.01),#45237,
'DISTANCE_ACCURACY_VALUE',
'Maximum model space distance between geometric entities at asserted c
onnectivities');
#45214=UNCERTAINTY_MEASURE_WITH_UNIT(LENGTH_MEASURE(0.01),#45237,
'DISTANCE_ACCURACY_VALUE',
'Maximum model space distance between geometric entities at asserted c
onnectivities');
#45224=(
GEOMETRIC_REPRESENTATION_CONTEXT(3)
GLOBAL_UNCERTAINTY_ASSIGNED_CONTEXT((#45202))
GLOBAL_UNIT_ASSIGNED_CONTEXT((#45237,#45239,#45240))
REPRESENTATION_CONTEXT('','3D')
);
#45236=(
GEOMETRIC_REPRESENTATION_CONTEXT(3)
GLOBAL_UNCERTAINTY_ASSIGNED_CONTEXT((#45214))
GLOBAL_UNIT_ASSIGNED_CONTEXT((#45237,#45239,#45240))
REPRESENTATION_CONTEXT('','3D')
);
#45237=(
LENGTH_UNIT()
NAMED_UNIT(*)
SI_UNIT(.MILLI.,.METRE.)
);
#45239=(
NAMED_UNIT(*)
PLANE_ANGLE_UNIT()
SI_UNIT($,.RADIAN.)
);
#45240=(
NAMED_UNIT(*)
SI_UNIT($,.STERADIAN.)
SOLID_ANGLE_UNIT()
);
#45250=SHAPE_DEFINITION_REPRESENTATION(#45271,#45322);
#45271=PRODUCT_DEFINITION_SHAPE('',$,#45344);
#45322=SHAPE_REPRESENTATION('',(#17253),#45224);
#45334=PRODUCT_DEFINITION_CONTEXT('part definition',#45399,'design');
#45344=PRODUCT_DEFINITION('2026-10-25-23-38-20-461',
'11_Handle_Pin_D6x22',#45365,#45334);
#45365=PRODUCT_DEFINITION_FORMATION('',$,#45410);
#45399=APPLICATION_CONTEXT(
'Core Data for Automotive Mechanical Design Process');
#45400=PRODUCT_CONTEXT('part definition',#45399,'mechanical');
#45410=PRODUCT('2026-10-25-23-38-20-461','11_Handle_Pin_D6x22',$,(#45400));
#45478=COLOUR_RGB('Grey',0.48,0.52,0.57);
#45479=FILL_AREA_STYLE_COLOUR('',#45478);
#45480=FILL_AREA_STYLE('',(#45479));
#45481=SURFACE_STYLE_FILL_AREA(#45480);
#45482=SURFACE_SIDE_STYLE('',(#45481));
#45483=SURFACE_STYLE_USAGE(.BOTH.,#45482);
#45484=PRESENTATION_STYLE_ASSIGNMENT((#45483));
ENDSEC;
END-ISO-10303-21;
